ISO-10303-21;
HEADER;
FILE_DESCRIPTION (('STEP AP214'),
    '1' );
FILE_NAME ('groove pin 01_iso_ISO 8739-M8x45-St.step',
    '2026-10-20T14:49:59',
    ( '' ),
    ( '' ),
    'SwSTEP 2.0',
    'SolidWorks 2025',
    '' );
FILE_SCHEMA (( 'AUTOMOTIVE_DESIGN' ));
ENDSEC;

DATA;
#19=VECTOR ( 'NONE', #6137, 1000.000000000000114 ) ;
#22=FACE_OUTER_BOUND ( 'NONE', #5382, .T. ) ;
#34=VERTEX_POINT ( 'NONE', #5261 ) ;
#125=VERTEX_POINT ( 'NONE', #7868 ) ;
#155=EDGE_CURVE ( 'NONE', #5994, #6514, #9956, .T. ) ;
#171=EDGE_CURVE ( 'NONE', #8144, #3030, #5631, .T. ) ;
#221=CARTESIAN_POINT ( 'NONE',  ( -0.8557715602033003632, -3.117691453623970599, -1.800000000000014921 ) ) ;
#264=VERTEX_POINT ( 'NONE', #1663 ) ;
#268=DIRECTION ( 'NONE',  ( -0.9805806756909200006, 0.000000000000000000, 0.1961161351381848494 ) ) ;
#289=VERTEX_POINT ( 'NONE', #2558 ) ;
#304=CARTESIAN_POINT ( 'NONE',  ( -39.66851723004002395, -4.408728476930471151E-16, 3.600000000000004530 ) ) ;
#308=PLANE ( 'NONE',  #2610 ) ;
#310=CARTESIAN_POINT ( 'NONE',  ( -40.33539666817951996, -3.418469287038251814, -2.079037510735993521 ) ) ;
#315=ORIENTED_EDGE ( 'NONE', *, *, #3953, .F. ) ;
#322=CARTESIAN_POINT ( 'NONE',  ( -1.071796769724492338, 3.319229491889297279, -2.232199717805803285 ) ) ;
#326=CARTESIAN_POINT ( 'NONE',  ( -38.96131932220313132, -3.592756407884938330, -1.758437202063725779 ) ) ;
#369=DIRECTION ( 'NONE',  ( 0.000000000000000000, 1.224646799147353207E-16, -1.000000000000000000 ) ) ;
#370=FACE_OUTER_BOUND ( 'NONE', #8957, .T. ) ;
#387=EDGE_CURVE ( 'NONE', #9162, #3341, #2763, .T. ) ;
#423=LINE ( 'NONE', #8528, #19 ) ;
#439=ORIENTED_EDGE ( 'NONE', *, *, #3690, .T. ) ;
#441=EDGE_CURVE ( 'NONE', #6928, #4613, #975, .T. ) ;
#444=DIRECTION ( 'NONE',  ( 1.000000000000000000, 0.000000000000000000, 0.000000000000000000 ) ) ;
#460=CARTESIAN_POINT ( 'NONE',  ( -40.99999999999999289, -3.464101615137750834, -2.000000000000019096 ) ) ;
#481=LINE ( 'NONE', #8373, #6459 ) ;
#501=ORIENTED_EDGE ( 'NONE', *, *, #3328, .F. ) ;
#503=CARTESIAN_POINT ( 'NONE',  ( -117.0000000000000000, -3.592756407884938330, -1.758437202063728666 ) ) ;
#506=AXIS2_PLACEMENT_3D ( 'NONE', #5972, #369, #2849 ) ;
#513=EDGE_LOOP ( 'NONE', ( #4202, #3563, #1283, #1400 ) ) ;
#559=FACE_OUTER_BOUND ( 'NONE', #2056, .T. ) ;
#597=ORIENTED_EDGE ( 'NONE', *, *, #4012, .F. ) ;
#607=ORIENTED_EDGE ( 'NONE', *, *, #10176, .F. ) ;
#608=DIRECTION ( 'NONE',  ( 1.000000000000000000, -1.000802005371234881E-16, 6.116012255046435111E-17 ) ) ;
#630=AXIS2_PLACEMENT_3D ( 'NONE', #7481, #3400, #1118 ) ;
#632=AXIS2_PLACEMENT_3D ( 'NONE', #2833, #3634, #7710 ) ;
#672=DIRECTION ( 'NONE',  ( 0.000000000000000000, 0.5735764363510477137, -0.8191520442889906883 ) ) ;
#674=ORIENTED_EDGE ( 'NONE', *, *, #2905, .T. ) ;
#689=CARTESIAN_POINT ( 'NONE',  ( -117.0000000000000000, 3.592756407884963643, -1.758437202063677596 ) ) ;
#706=ADVANCED_FACE ( 'NONE', ( #4191 ), #8961, .T. ) ;
#709=ORIENTED_EDGE ( 'NONE', *, *, #9893, .T. ) ;
#722=CIRCLE ( 'NONE', #10375, 4.000000000000000000 ) ;
#723=VERTEX_POINT ( 'NONE', #221 ) ;
#727=PLANE ( 'NONE',  #5508 ) ;
#758=ORIENTED_EDGE ( 'NONE', *, *, #3924, .F. ) ;
#772=EDGE_CURVE ( 'NONE', #1040, #1722, #2099, .T. ) ;
#784=ORIENTED_EDGE ( 'NONE', *, *, #5041, .F. ) ;
#799=CARTESIAN_POINT ( 'NONE',  ( -40.99999999999999289, -5.556536133988210224E-16, 4.000000000000005329 ) ) ;
#804=EDGE_CURVE ( 'NONE', #6696, #289, #4348, .T. ) ;
#814=DIRECTION ( 'NONE',  ( 0.000000000000000000, 0.000000000000000000, 1.000000000000000000 ) ) ;
#831=CARTESIAN_POINT ( 'NONE',  ( -37.01000625782472753, 0.000000000000000000, 0.000000000000000000 ) ) ;
#880=DIRECTION ( 'NONE',  ( 0.000000000000000000, 1.000000000000000000, 0.000000000000000000 ) ) ;
#895=CARTESIAN_POINT ( 'NONE',  ( -40.99999999999999289, 3.464101615137777923, -1.999999999999970468 ) ) ;
#900=CIRCLE ( 'NONE', #1237, 3.999999999999999112 ) ;
#962=ORIENTED_EDGE ( 'NONE', *, *, #8063, .T. ) ;
#975=CIRCLE ( 'NONE', #7407, 8.000000000000000000 ) ;
#980=DIRECTION ( 'NONE',  ( -7.016001027857739179E-17, -0.8191520442889906883, -0.5735764363510477137 ) ) ;
#985=AXIS2_PLACEMENT_3D ( 'NONE', #3858, #8781, #7242 ) ;
#1008=ORIENTED_EDGE ( 'NONE', *, *, #7644, .F. ) ;
#1040=VERTEX_POINT ( 'NONE', #6300 ) ;
#1047=LINE ( 'NONE', #4130, #10225 ) ;
#1054=ORIENTED_EDGE ( 'NONE', *, *, #2979, .T. ) ;
#1059=CARTESIAN_POINT ( 'NONE',  ( -40.33539666817950575, 0.09126465619898900539, 4.000000000000000000 ) ) ;
#1084=( GEOMETRIC_REPRESENTATION_CONTEXT ( 3 ) GLOBAL_UNCERTAINTY_ASSIGNED_CONTEXT ( ( #4932 ) ) GLOBAL_UNIT_ASSIGNED_CONTEXT ( ( #1252, #7667, #5170 ) ) REPRESENTATION_CONTEXT ( 'NONE', 'WORKASPACE' ) );
#1090=SPHERICAL_SURFACE ( 'NONE', #4333, 8.000000000000000000 ) ;
#1118=DIRECTION ( 'NONE',  ( 0.000000000000000000, 0.000000000000000000, 1.000000000000000000 ) ) ;
#1120=ORIENTED_EDGE ( 'NONE', *, *, #5629, .T. ) ;
#1132=DIRECTION ( 'NONE',  ( -1.000000000000000000, -0.000000000000000000, -0.000000000000000000 ) ) ;
#1134=ORIENTED_EDGE ( 'NONE', *, *, #9097, .T. ) ;
#1180=ORIENTED_EDGE ( 'NONE', *, *, #9874, .T. ) ;
#1237=AXIS2_PLACEMENT_3D ( 'NONE', #2653, #9877, #8163 ) ;
#1252=( LENGTH_UNIT ( ) NAMED_UNIT ( * ) SI_UNIT ( .MILLI., .METRE. ) );
#1263=DIRECTION ( 'NONE',  ( -1.000000000000000000, -0.000000000000000000, -0.000000000000000000 ) ) ;
#1270=DIRECTION ( 'NONE',  ( 0.000000000000000000, 0.4226182617406934461, 0.9063077870366527122 ) ) ;
#1283=ORIENTED_EDGE ( 'NONE', *, *, #6820, .F. ) ;
#1292=CARTESIAN_POINT ( 'NONE',  ( -40.99999999999999289, 3.464101615137777923, -1.999999999999970468 ) ) ;
#1373=EDGE_LOOP ( 'NONE', ( #7670, #9589 ) ) ;
#1383=CARTESIAN_POINT ( 'NONE',  ( -117.0000000000000000, 0.000000000000000000, 0.000000000000000000 ) ) ;
#1384=VECTOR ( 'NONE', #4482, 1000.000000000000227 ) ;
#1388=ORIENTED_EDGE ( 'NONE', *, *, #5728, .T. ) ;
#1400=ORIENTED_EDGE ( 'NONE', *, *, #2979, .F. ) ;
#1450=ORIENTED_EDGE ( 'NONE', *, *, #6573, .T. ) ;
#1461=DIRECTION ( 'NONE',  ( -0.9805806756909200006, -0.1698415551216896080, -0.09805806756909324351 ) ) ;
#1472=ORIENTED_EDGE ( 'NONE', *, *, #9893, .F. ) ;
#1482=ORIENTED_EDGE ( 'NONE', *, *, #10425, .F. ) ;
#1489=CARTESIAN_POINT ( 'NONE',  ( -1.071796769724492338, 0.000000000000000000, 0.000000000000000000 ) ) ;
#1494=DIRECTION ( 'NONE',  ( 0.1124875939035006184, 0.07750954751060692982, -0.9906254646749710346 ) ) ;
#1509=STYLED_ITEM('',(#10518),#2958);
#1529=ADVANCED_FACE ( 'NONE', ( #3007 ), #2321, .T. ) ;
#1540=DIRECTION ( 'NONE',  ( -1.000000000000000000, -0.000000000000000000, -0.000000000000000000 ) ) ;
#1543=DIRECTION ( 'NONE',  ( -0.9936146452197298640, 0.000000000000000000, -0.1128270216077272570 ) ) ;
#1616=CARTESIAN_POINT ( 'NONE',  ( -39.66851723004002395, -4.408728476930471151E-16, 3.600000000000004530 ) ) ;
#1618=CIRCLE ( 'NONE', #7049, 0.4000000000000000222 ) ;
#1627=EDGE_CURVE ( 'NONE', #8144, #9162, #5733, .T. ) ;
#1640=EDGE_LOOP ( 'NONE', ( #4239, #7288, #2353 ) ) ;
#1659=( NAMED_UNIT ( * ) PLANE_ANGLE_UNIT ( ) SI_UNIT ( $, .RADIAN. ) );
#1663=CARTESIAN_POINT ( 'NONE',  ( -45.00000000000000000, 0.4000000000000000222, 0.000000000000000000 ) ) ;
#1680=SPHERICAL_SURFACE ( 'NONE', #2071, 8.000000000000000000 ) ;
#1704=CARTESIAN_POINT ( 'NONE',  ( -8.000000000000000000, 0.1799657291978528917, -2.057017697435775005 ) ) ;
#1712=CARTESIAN_POINT ( 'NONE',  ( -39.00428932080996702, 3.095342794014916965, -1.752073144804183080 ) ) ;
#1722=VERTEX_POINT ( 'NONE', #7700 ) ;
#1732=FACE_OUTER_BOUND ( 'NONE', #6195, .T. ) ;
#1816=VERTEX_POINT ( 'NONE', #10355 ) ;
#1832=SPHERICAL_SURFACE ( 'NONE', #632, 8.000000000000000000 ) ;
#1840=( GEOMETRIC_REPRESENTATION_CONTEXT ( 3 ) GLOBAL_UNCERTAINTY_ASSIGNED_CONTEXT ( ( #5531 ) ) GLOBAL_UNIT_ASSIGNED_CONTEXT ( ( #7330, #1659, #3296 ) ) REPRESENTATION_CONTEXT ( 'NONE', 'WORKASPACE' ) );
#1856=CARTESIAN_POINT ( 'NONE',  ( -38.96131932220313132, 0.2735269159956709717, 3.990636919869543942 ) ) ;
#1878=ORIENTED_EDGE ( 'NONE', *, *, #804, .F. ) ;
#1880=ORIENTED_EDGE ( 'NONE', *, *, #6629, .F. ) ;
#1896=CARTESIAN_POINT ( 'NONE',  ( -45.00000000000000000, -0.4000000000000000222, -2.694222958124179965E-16 ) ) ;
#1917=CARTESIAN_POINT ( 'NONE',  ( -117.0000000000000000, 3.319229491889298167, -2.232199717805803729 ) ) ;
#1936=DIRECTION ( 'NONE',  ( -0.000000000000000000, 0.000000000000000000, -1.000000000000000000 ) ) ;
#1952=ORIENTED_EDGE ( 'NONE', *, *, #6956, .T. ) ;
#1975=CIRCLE ( 'NONE', #8064, 3.999999999999999112 ) ;
#1984=CIRCLE ( 'NONE', #9268, 7.728925574020642841 ) ;
#1986=VECTOR ( 'NONE', #608, 1000.000000000000000 ) ;
#2001=CARTESIAN_POINT ( 'NONE',  ( -43.93820948810023452, 0.000000000000000000, 4.000000000000000000 ) ) ;
#2022=ADVANCED_FACE ( 'NONE', ( #9329 ), #10288, .F. ) ;
#2038=FACE_OUTER_BOUND ( 'NONE', #9675, .T. ) ;
#2040=ORIENTED_EDGE ( 'NONE', *, *, #441, .F. ) ;
#2056=EDGE_LOOP ( 'NONE', ( #10376, #7932, #1952 ) ) ;
#2059=CARTESIAN_POINT ( 'NONE',  ( -39.65624476065124782, -3.117691453623975484, -1.800000000000017586 ) ) ;
#2070=AXIS2_PLACEMENT_3D ( 'NONE', #10310, #6418, #10356 ) ;
#2071=AXIS2_PLACEMENT_3D ( 'NONE', #831, #9802, #880 ) ;
#2095=EDGE_LOOP ( 'NONE', ( #1134, #4062, #1388, #6491, #7589 ) ) ;
#2099=( BOUNDED_CURVE ( )  B_SPLINE_CURVE ( 3, ( #1856, #5086, #1059, #4291 ),
 .UNSPECIFIED., .F., .F. ) 
 B_SPLINE_CURVE_WITH_KNOTS ( ( 4, 4 ),
 ( 5.245636577995398397, 5.314071712302153472 ),
 .UNSPECIFIED. ) 
 CURVE ( )  GEOMETRIC_REPRESENTATION_ITEM ( )  RATIONAL_B_SPLINE_CURVE ( ( 1.000000000000000000, 0.9996097574442918132, 0.9996097574442918132, 1.000000000000000000 ) ) 
 REPRESENTATION_ITEM ( '' )  );
#2101=AXIS2_PLACEMENT_3D ( 'NONE', #5351, #1132, #9189 ) ;
#2146=VERTEX_POINT ( 'NONE', #3066 ) ;
#2168=EDGE_LOOP ( 'NONE', ( #6812, #9545, #7693, #8510 ) ) ;
#2195=ORIENTED_EDGE ( 'NONE', *, *, #4051, .T. ) ;
#2229=AXIS2_PLACEMENT_3D ( 'NONE', #5948, #10096, #2878 ) ;
#2237=VECTOR ( 'NONE', #3122, 1000.000000000000000 ) ;
#2246=AXIS2_PLACEMENT_3D ( 'NONE', #5492, #10275, #7334 ) ;
#2265=APPLICATION_CONTEXT ( 'automotive_design' ) ;
#2267=DIRECTION ( 'NONE',  ( 0.1124875939035003825, 0.8966615917995841567, 0.4281874951574803356 ) ) ;
#2299=LINE ( 'NONE', #503, #7810 ) ;
#2316=ORIENTED_EDGE ( 'NONE', *, *, #5596, .T. ) ;
#2321=PLANE ( 'NONE',  #10432 ) ;
#2329=ORIENTED_EDGE ( 'NONE', *, *, #9097, .F. ) ;
#2336=VECTOR ( 'NONE', #3062, 1000.000000000000000 ) ;
#2353=ORIENTED_EDGE ( 'NONE', *, *, #8199, .T. ) ;
#2421=DIRECTION ( 'NONE',  ( 0.000000000000000000, 1.224646799147353207E-16, -1.000000000000000000 ) ) ;
#2453=CARTESIAN_POINT ( 'NONE',  ( -43.93820948810023452, 0.000000000000000000, 0.000000000000000000 ) ) ;
#2454=PLANE ( 'NONE',  #2246 ) ;
#2504=( BOUNDED_CURVE ( )  B_SPLINE_CURVE ( 3, ( #1292, #4526, #5900, #9138 ),
 .UNSPECIFIED., .F., .T. ) 
 B_SPLINE_CURVE_WITH_KNOTS ( ( 4, 4 ),
 ( 0.9691135948774319830, 1.037548729184187613 ),
 .UNSPECIFIED. ) 
 CURVE ( )  GEOMETRIC_REPRESENTATION_ITEM ( )  RATIONAL_B_SPLINE_CURVE ( ( 1.000000000000000000, 0.9996097574442918132, 0.9996097574442918132, 1.000000000000000000 ) ) 
 REPRESENTATION_ITEM ( '' )  );
#2521=EDGE_CURVE ( 'NONE', #7666, #264, #4203, .T. ) ;
#2558=CARTESIAN_POINT ( 'NONE',  ( -39.00000000000000000, -3.117691453623975484, -1.800000000000017586 ) ) ;
#2583=EDGE_CURVE ( 'NONE', #3341, #9180, #5721, .T. ) ;
#2588=LINE ( 'NONE', #4232, #3413 ) ;
#2595=CARTESIAN_POINT ( 'NONE',  ( -0.8557715602033003632, -6.505213034913026604E-16, 3.600000000000000977 ) ) ;
#2602=CARTESIAN_POINT ( 'NONE',  ( -117.0000000000000000, 0.2735269159956686957, 3.990636919869546606 ) ) ;
#2608=LINE ( 'NONE', #5832, #6751 ) ;
#2610=AXIS2_PLACEMENT_3D ( 'NONE', #9199, #6758, #9309 ) ;
#2628=ADVANCED_FACE ( 'NONE', ( #6489 ), #3960, .F. ) ;
#2643=DIRECTION ( 'NONE',  ( 0.08084652178105143638, 0.5716988695978858503, 0.8164706010729385621 ) ) ;
#2648=ORIENTED_EDGE ( 'NONE', *, *, #3265, .T. ) ;
#2653=CARTESIAN_POINT ( 'NONE',  ( -1.071796769724492338, 0.000000000000000000, 0.000000000000000000 ) ) ;
#2684=EDGE_CURVE ( 'NONE', #9349, #10166, #9982, .T. ) ;
#2729=DIRECTION ( 'NONE',  ( -1.000000000000000000, -0.000000000000000000, -0.000000000000000000 ) ) ;
#2746=CARTESIAN_POINT ( 'NONE',  ( -39.65557114539780059, -3.552635616211478720, -1.840410121656805620 ) ) ;
#2762=EDGE_CURVE ( 'NONE', #3747, #9349, #7552, .T. ) ;
#2763=LINE ( 'NONE', #1917, #10462 ) ;
#2805=CARTESIAN_POINT ( 'NONE',  ( -40.99999999999999289, -3.464101615137750834, -2.000000000000019096 ) ) ;
#2826=ORIENTED_EDGE ( 'NONE', *, *, #3953, .T. ) ;
#2833=CARTESIAN_POINT ( 'NONE',  ( -37.01000625782472753, 0.000000000000000000, 0.000000000000000000 ) ) ;
#2843=( BOUNDED_CURVE ( )  B_SPLINE_CURVE ( 3, ( #10020, #2746, #4550, #2961 ),
 .UNSPECIFIED., .F., .F. ) 
 B_SPLINE_CURVE_WITH_KNOTS ( ( 4, 4 ),
 ( 5.245636577995398397, 5.314071712302153472 ),
 .UNSPECIFIED. ) 
 CURVE ( )  GEOMETRIC_REPRESENTATION_ITEM ( )  RATIONAL_B_SPLINE_CURVE ( ( 1.000000000000000000, 0.9996097574442918132, 0.9996097574442918132, 1.000000000000000000 ) ) 
 REPRESENTATION_ITEM ( '' )  );
#2849=DIRECTION ( 'NONE',  ( 0.000000000000000000, 1.000000000000000000, 1.224646799147353207E-16 ) ) ;
#2858=EDGE_LOOP ( 'NONE', ( #4561, #6727, #4172 ) ) ;
#2863=PLANE ( 'NONE',  #5875 ) ;
#2867=EDGE_LOOP ( 'NONE', ( #709, #4008, #439 ) ) ;
#2878=DIRECTION ( 'NONE',  ( 0.000000000000000000, -0.9961946980917457672, 0.08715574274765484908 ) ) ;
#2886=CARTESIAN_POINT ( 'NONE',  ( -8.000000000000000000, 0.000000000000000000, 0.000000000000000000 ) ) ;
#2905=EDGE_CURVE ( 'NONE', #10166, #9506, #2608, .T. ) ;
#2908=( BOUNDED_CURVE ( )  B_SPLINE_CURVE ( 3, ( #799, #5574, #8056, #9508 ),
 .UNSPECIFIED., .F., .T. ) 
 B_SPLINE_CURVE_WITH_KNOTS ( ( 4, 4 ),
 ( 0.9691135948774318720, 1.037548729184187168 ),
 .UNSPECIFIED. ) 
 CURVE ( )  GEOMETRIC_REPRESENTATION_ITEM ( )  RATIONAL_B_SPLINE_CURVE ( ( 1.000000000000000000, 0.9996097574442918132, 0.9996097574442918132, 1.000000000000000000 ) ) 
 REPRESENTATION_ITEM ( '' )  );
#2909=ORIENTED_EDGE ( 'NONE', *, *, #10315, .F. ) ;
#2958=MANIFOLD_SOLID_BREP ( 'CirPattern1', #4186 ) ;
#2961=CARTESIAN_POINT ( 'NONE',  ( -40.99999999999999289, -3.464101615137750834, -2.000000000000019096 ) ) ;
#2975=PRODUCT_DEFINITION_SHAPE ( 'NONE', 'NONE',  #8524 ) ;
#2976=EDGE_LOOP ( 'NONE', ( #1482, #1120, #9266, #1472, #5433, #9665, #2316, #2648, #674, #5990, #5400, #3667, #7202 ) ) ;
#2979=EDGE_CURVE ( 'NONE', #3030, #7406, #3193, .T. ) ;
#2992=AXIS2_PLACEMENT_3D ( 'NONE', #8735, #2421, #7201 ) ;
#3007=FACE_OUTER_BOUND ( 'NONE', #2858, .T. ) ;
#3012=CARTESIAN_POINT ( 'NONE',  ( -117.0000000000000000, -3.319229491889267081, -2.232199717805850803 ) ) ;
#3030=VERTEX_POINT ( 'NONE', #5674 ) ;
#3062=DIRECTION ( 'NONE',  ( -0.08084652178105139475, 0.5716988695978864055, -0.8164706010729381180 ) ) ;
#3066=CARTESIAN_POINT ( 'NONE',  ( -1.071796769724492338, 0.2735269159956686402, 3.990636919869545718 ) ) ;
#3086=DIRECTION ( 'NONE',  ( 1.000000000000000000, 1.112002228190260952E-16, 6.116012255046435111E-17 ) ) ;
#3122=DIRECTION ( 'NONE',  ( -1.000000000000000000, -0.000000000000000000, -0.000000000000000000 ) ) ;
#3128=CARTESIAN_POINT ( 'NONE',  ( -39.00428932080996702, 3.065011249696406370, -1.804608920635871749 ) ) ;
#3156=CIRCLE ( 'NONE', #2992, 8.000000000000000000 ) ;
#3193=CIRCLE ( 'NONE', #3544, 7.728925574020642841 ) ;
#3205=ORIENTED_EDGE ( 'NONE', *, *, #387, .F. ) ;
#3241=DIRECTION ( 'NONE',  ( -1.000000000000000000, -0.000000000000000000, -0.000000000000000000 ) ) ;
#3265=EDGE_CURVE ( 'NONE', #125, #10166, #4557, .T. ) ;
#3296=( NAMED_UNIT ( * ) SI_UNIT ( $, .STERADIAN. ) SOLID_ANGLE_UNIT ( ) );
#3328=EDGE_CURVE ( 'NONE', #6928, #125, #6421, .T. ) ;
#3341=VERTEX_POINT ( 'NONE', #322 ) ;
#3342=AXIS2_PLACEMENT_3D ( 'NONE', #2453, #8017, #814 ) ;
#3390=EDGE_CURVE ( 'NONE', #1816, #6696, #6345, .T. ) ;
#3400=DIRECTION ( 'NONE',  ( -1.000000000000000000, -0.000000000000000000, -0.000000000000000000 ) ) ;
#3413=VECTOR ( 'NONE', #2643, 1000.000000000000000 ) ;
#3430=ORIENTED_EDGE ( 'NONE', *, *, #3690, .F. ) ;
#3502=LINE ( 'NONE', #6839, #10026 ) ;
#3526=DIRECTION ( 'NONE',  ( 1.000000000000000000, -0.000000000000000000, -1.223202451009287022E-16 ) ) ;
#3529=VECTOR ( 'NONE', #5243, 1000.000000000000227 ) ;
#3544=AXIS2_PLACEMENT_3D ( 'NONE', #1704, #8014, #6422 ) ;
#3563=ORIENTED_EDGE ( 'NONE', *, *, #9874, .F. ) ;
#3577=ADVANCED_FACE ( 'NONE', ( #5164 ), #1832, .T. ) ;
#3618=ORIENTED_EDGE ( 'NONE', *, *, #10477, .F. ) ;
#3624=CARTESIAN_POINT ( 'NONE',  ( -1.071796769724492338, 3.592756407884963643, -1.758437202063677596 ) ) ;
#3628=FACE_OUTER_BOUND ( 'NONE', #8929, .T. ) ;
#3634=DIRECTION ( 'NONE',  ( -0.000000000000000000, 0.000000000000000000, -1.000000000000000000 ) ) ;
#3654=AXIS2_PLACEMENT_3D ( 'NONE', #9310, #9253, #10050 ) ;
#3664=DIRECTION ( 'NONE',  ( -1.000000000000000000, -0.000000000000000000, -0.000000000000000000 ) ) ;
#3666=DIRECTION ( 'NONE',  ( 0.000000000000000000, 0.5735764363510470476, 0.8191520442889910214 ) ) ;
#3667=ORIENTED_EDGE ( 'NONE', *, *, #5980, .F. ) ;
#3680=ADVANCED_BREP_SHAPE_REPRESENTATION ( '', ( #2958, #4601 ), #1084 ) ;
#3690=EDGE_CURVE ( 'NONE', #289, #7867, #8557, .T. ) ;
#3727=DIRECTION ( 'NONE',  ( -0.000000000000000000, 0.000000000000000000, 1.000000000000000000 ) ) ;
#3731=ADVANCED_FACE ( 'NONE', ( #559 ), #10364, .T. ) ;
#3747=VERTEX_POINT ( 'NONE', #8610 ) ;
#3784=CARTESIAN_POINT ( 'NONE',  ( -45.00000000000000000, 0.000000000000000000, 0.000000000000000000 ) ) ;
#3793=DIRECTION ( 'NONE',  ( 0.000000000000000000, -0.5660304919045651140, -0.8243843049417401980 ) ) ;
#3799=ORIENTED_EDGE ( 'NONE', *, *, #3328, .T. ) ;
#3858=CARTESIAN_POINT ( 'NONE',  ( -37.01000625782472753, 0.000000000000000000, 0.000000000000000000 ) ) ;
#3885=PLANE ( 'NONE',  #4656 ) ;
#3903=DIRECTION ( 'NONE',  ( 0.1124875939035004102, -0.8191520442889910214, 0.5624379695174998028 ) ) ;
#3917=CARTESIAN_POINT ( 'NONE',  ( -39.00428932080996702, -3.095342794014893428, -1.752073144804227933 ) ) ;
#3924=EDGE_CURVE ( 'NONE', #1040, #2146, #9016, .T. ) ;
#3940=LINE ( 'NONE', #7218, #6107 ) ;
#3953=EDGE_CURVE ( 'NONE', #289, #9495, #6582, .T. ) ;
#3960=PLANE ( 'NONE',  #6916 ) ;
#3962=DIRECTION ( 'NONE',  ( 0.000000000000000000, -0.4309225046084501631, 0.9023889377768214981 ) ) ;
#4008=ORIENTED_EDGE ( 'NONE', *, *, #804, .T. ) ;
#4012=EDGE_CURVE ( 'NONE', #723, #1816, #1984, .T. ) ;
#4021=ORIENTED_EDGE ( 'NONE', *, *, #4051, .F. ) ;
#4051=EDGE_CURVE ( 'NONE', #2146, #9349, #9449, .T. ) ;
#4062=ORIENTED_EDGE ( 'NONE', *, *, #155, .T. ) ;
#4107=ADVANCED_FACE ( 'NONE', ( #5246 ), #2863, .F. ) ;
#4130=CARTESIAN_POINT ( 'NONE',  ( -38.99999999999999289, -5.592496027482437178E-16, 3.600000000000004530 ) ) ;
#4133=EDGE_LOOP ( 'NONE', ( #758, #6777, #8041, #4021 ) ) ;
#4172=ORIENTED_EDGE ( 'NONE', *, *, #1627, .T. ) ;
#4186=CLOSED_SHELL ( 'NONE', ( #8290, #4903, #3577, #5929, #5410, #4875, #9200, #8777, #3731, #2628, #4107, #4621, #706, #2022, #6521, #9219, #1529, #5745, #7164 ) ) ;
#4191=FACE_OUTER_BOUND ( 'NONE', #4940, .T. ) ;
#4202=ORIENTED_EDGE ( 'NONE', *, *, #171, .F. ) ;
#4203=CIRCLE ( 'NONE', #985, 8.000000000000000000 ) ;
#4232=CARTESIAN_POINT ( 'NONE',  ( -39.00436953563450970, -0.03089877619826558730, 3.555871974361681342 ) ) ;
#4239=ORIENTED_EDGE ( 'NONE', *, *, #10239, .T. ) ;
#4247=CARTESIAN_POINT ( 'NONE',  ( -40.33539666817951996, 3.418469287038280680, -2.079037510735945560 ) ) ;
#4291=CARTESIAN_POINT ( 'NONE',  ( -40.99999999999999289, -5.556536133988210224E-16, 4.000000000000005329 ) ) ;
#4299=CARTESIAN_POINT ( 'NONE',  ( -39.65557114539780059, 3.370159726842552050, -2.156467633200104483 ) ) ;
#4333=AXIS2_PLACEMENT_3D ( 'NONE', #2886, #1936, #6117 ) ;
#4348=LINE ( 'NONE', #7741, #3529 ) ;
#4364=VECTOR ( 'NONE', #9825, 1000.000000000000114 ) ;
#4370=ORIENTED_EDGE ( 'NONE', *, *, #387, .T. ) ;
#4377=VERTEX_POINT ( 'NONE', #895 ) ;
#4383=CARTESIAN_POINT ( 'NONE',  ( -38.96131932220313132, -3.319229491889264416, -2.232199717805851691 ) ) ;
#4399=AXIS2_PLACEMENT_3D ( 'NONE', #4441, #1263, #9267 ) ;
#4441=CARTESIAN_POINT ( 'NONE',  ( -1.071796769724492338, 0.000000000000000000, 0.000000000000000000 ) ) ;
#4442=DIRECTION ( 'NONE',  ( 0.000000000000000000, 0.000000000000000000, 1.000000000000000000 ) ) ;
#4464=VERTEX_POINT ( 'NONE', #1896 ) ;
#4482=DIRECTION ( 'NONE',  ( -0.08084652178105136699, -0.9929337167712568579, -0.08687044385015690873 ) ) ;
#4510=DIRECTION ( 'NONE',  ( 0.000000000000000000, 0.5735764363510471586, 0.8191520442889911324 ) ) ;
#4511=CARTESIAN_POINT ( 'NONE',  ( -38.96131932220313132, 3.319229491889295502, -2.232199717805805061 ) ) ;
#4526=CARTESIAN_POINT ( 'NONE',  ( -40.33539666817953417, 3.509733943237267617, -1.920962489263991158 ) ) ;
#4550=CARTESIAN_POINT ( 'NONE',  ( -40.33539666817950575, -3.509733943237241416, -1.920962489264039785 ) ) ;
#4557=CIRCLE ( 'NONE', #4399, 3.999999999999999112 ) ;
#4559=CARTESIAN_POINT ( 'NONE',  ( -8.000000000000000000, -1.871412446612475522, 0.8726539554219646666 ) ) ;
#4561=ORIENTED_EDGE ( 'NONE', *, *, #5641, .T. ) ;
#4601=AXIS2_PLACEMENT_3D ( 'NONE', #8586, #5983, #5928 ) ;
#4612=CYLINDRICAL_SURFACE ( 'NONE', #7703, 4.000000000000000000 ) ;
#4613=VERTEX_POINT ( 'NONE', #9648 ) ;
#4616=ORIENTED_EDGE ( 'NONE', *, *, #2521, .T. ) ;
#4621=ADVANCED_FACE ( 'NONE', ( #10334 ), #727, .T. ) ;
#4636=CARTESIAN_POINT ( 'NONE',  ( -39.00000000000000000, -3.117691453623975484, -1.800000000000017586 ) ) ;
#4639=ORIENTED_EDGE ( 'NONE', *, *, #1627, .F. ) ;
#4656=AXIS2_PLACEMENT_3D ( 'NONE', #3128, #1494, #1543 ) ;
#4662=LINE ( 'NONE', #689, #2237 ) ;
#4687=CARTESIAN_POINT ( 'NONE',  ( -39.65624476065125492, 3.117691453623999909, -1.799999999999972955 ) ) ;
#4697=AXIS2_PLACEMENT_3D ( 'NONE', #6950, #6093, #3666 ) ;
#4713=AXIS2_PLACEMENT_3D ( 'NONE', #6339, #4791, #9684 ) ;
#4791=DIRECTION ( 'NONE',  ( -1.000000000000000000, -0.000000000000000000, -0.000000000000000000 ) ) ;
#4816=EDGE_CURVE ( 'NONE', #264, #4464, #5514, .T. ) ;
#4843=DIRECTION ( 'NONE',  ( -7.016001027857739179E-17, -0.8191520442889906883, -0.5735764363510477137 ) ) ;
#4865=AXIS2_PLACEMENT_3D ( 'NONE', #7370, #9875, #5824 ) ;
#4867=ORIENTED_EDGE ( 'NONE', *, *, #7734, .F. ) ;
#4875=ADVANCED_FACE ( 'NONE', ( #2038 ), #6067, .T. ) ;
#4903=ADVANCED_FACE ( 'NONE', ( #6923 ), #1090, .T. ) ;
#4932=UNCERTAINTY_MEASURE_WITH_UNIT (LENGTH_MEASURE( 1.000000000000000082E-05 ), #1252, 'distance_accuracy_value', 'NONE');
#4940=EDGE_LOOP ( 'NONE', ( #6739, #3430, #2826 ) ) ;
#4959=ORIENTED_EDGE ( 'NONE', *, *, #3390, .F. ) ;
#4974=DIRECTION ( 'NONE',  ( -1.000000000000000000, -0.000000000000000000, -0.000000000000000000 ) ) ;
#5020=CIRCLE ( 'NONE', #630, 3.999999999999999112 ) ;
#5041=EDGE_CURVE ( 'NONE', #4464, #264, #1618, .T. ) ;
#5044=PRODUCT_DEFINITION_CONTEXT ( 'detailed design', #2265, 'design' ) ;
#5064=CARTESIAN_POINT ( 'NONE',  ( -43.93820948810023452, 0.000000000000000000, 0.000000000000000000 ) ) ;
#5086=CARTESIAN_POINT ( 'NONE',  ( -39.65557114539779349, 0.1824758893689546746, 3.996877754856924536 ) ) ;
#5093=ORIENTED_EDGE ( 'NONE', *, *, #2684, .T. ) ;
#5103=DIRECTION ( 'NONE',  ( -1.000000000000000000, -0.000000000000000000, -0.000000000000000000 ) ) ;
#5128=AXIS2_PLACEMENT_3D ( 'NONE', #1489, #1540, #10444 ) ;
#5164=FACE_OUTER_BOUND ( 'NONE', #2095, .T. ) ;
#5167=DIRECTION ( 'NONE',  ( -7.061912783291096091E-17, 0.08715574274765486296, 0.9961946980917459893 ) ) ;
#5170=( NAMED_UNIT ( * ) SI_UNIT ( $, .STERADIAN. ) SOLID_ANGLE_UNIT ( ) );
#5203=CARTESIAN_POINT ( 'NONE',  ( -8.000000000000000000, 0.000000000000000000, 0.000000000000000000 ) ) ;
#5207=VECTOR ( 'NONE', #7374, 1000.000000000000000 ) ;
#5243=DIRECTION ( 'NONE',  ( -0.08084652178105138087, 0.4212348471733671218, 0.9033410449230877548 ) ) ;
#5244=DIRECTION ( 'NONE',  ( -1.000000000000000000, -0.000000000000000000, -0.000000000000000000 ) ) ;
#5246=FACE_OUTER_BOUND ( 'NONE', #4133, .T. ) ;
#5261=CARTESIAN_POINT ( 'NONE',  ( -38.96131932220313132, 3.592756407884963199, -1.758437202063674487 ) ) ;
#5274=ORIENTED_EDGE ( 'NONE', *, *, #3924, .T. ) ;
#5297=CARTESIAN_POINT ( 'NONE',  ( -39.66851723004002395, -4.408728476930471151E-16, 3.600000000000004530 ) ) ;
#5310=PLANE ( 'NONE',  #5522 ) ;
#5325=ORIENTED_EDGE ( 'NONE', *, *, #5641, .F. ) ;
#5326=ORIENTED_EDGE ( 'NONE', *, *, #5728, .F. ) ;
#5337=CYLINDRICAL_SURFACE ( 'NONE', #7179, 4.000000000000000000 ) ;
#5351=CARTESIAN_POINT ( 'NONE',  ( -43.93820948810023452, 0.000000000000000000, 0.000000000000000000 ) ) ;
#5380=SHAPE_DEFINITION_REPRESENTATION ( #2975, #6905 ) ;
#5382=EDGE_LOOP ( 'NONE', ( #3205, #4639, #5523, #1008 ) ) ;
#5400=ORIENTED_EDGE ( 'NONE', *, *, #10477, .T. ) ;
#5410=ADVANCED_FACE ( 'NONE', ( #10357 ), #5310, .F. ) ;
#5433=ORIENTED_EDGE ( 'NONE', *, *, #9503, .F. ) ;
#5485=PRODUCT_CONTEXT ( 'NONE', #7680, 'mechanical' ) ;
#5492=CARTESIAN_POINT ( 'NONE',  ( -39.65624476065125492, 3.117691453623999909, -1.799999999999972955 ) ) ;
#5497=FACE_OUTER_BOUND ( 'NONE', #513, .T. ) ;
#5508=AXIS2_PLACEMENT_3D ( 'NONE', #3917, #6291, #8832 ) ;
#5514=CIRCLE ( 'NONE', #6874, 0.4000000000000000222 ) ;
#5522=AXIS2_PLACEMENT_3D ( 'NONE', #3784, #8551, #9512 ) ;
#5523=ORIENTED_EDGE ( 'NONE', *, *, #171, .T. ) ;
#5531=UNCERTAINTY_MEASURE_WITH_UNIT (LENGTH_MEASURE( 1.000000000000000082E-05 ), #7330, 'distance_accuracy_value', 'NONE');
#5533=AXIS2_PLACEMENT_3D ( 'NONE', #7870, #3903, #3793 ) ;
#5574=CARTESIAN_POINT ( 'NONE',  ( -40.33539666817951996, -0.09126465619898782577, 4.000000000000000888 ) ) ;
#5596=EDGE_CURVE ( 'NONE', #8325, #125, #1975, .T. ) ;
#5629=EDGE_CURVE ( 'NONE', #9180, #1816, #5020, .T. ) ;
#5631=LINE ( 'NONE', #4687, #1986 ) ;
#5641=EDGE_CURVE ( 'NONE', #9162, #4377, #7927, .T. ) ;
#5674=CARTESIAN_POINT ( 'NONE',  ( -0.8557715602033003632, 3.117691453623996356, -1.799999999999970957 ) ) ;
#5681=PRODUCT ( 'groove pin 01_iso_ISO 8739-M8x45-St', 'groove pin 01_iso_ISO 8739-M8x45-St', '', ( #5485 ) ) ;
#5721=CIRCLE ( 'NONE', #4713, 3.999999999999999112 ) ;
#5728=EDGE_CURVE ( 'NONE', #6514, #4464, #3156, .T. ) ;
#5733=LINE ( 'NONE', #1712, #6526 ) ;
#5745=ADVANCED_FACE ( 'NONE', ( #5497 ), #7988, .F. ) ;
#5751=DIRECTION ( 'NONE',  ( 0.000000000000000000, 0.000000000000000000, 1.000000000000000000 ) ) ;
#5769=DIRECTION ( 'NONE',  ( 0.000000000000000000, 0.000000000000000000, 1.000000000000000000 ) ) ;
#5791=CIRCLE ( 'NONE', #2070, 7.728925574020642841 ) ;
#5824=DIRECTION ( 'NONE',  ( -0.9936146452197298640, 0.000000000000000000, -0.1128270216077269933 ) ) ;
#5825=CARTESIAN_POINT ( 'NONE',  ( -43.93820948810023452, 0.000000000000000000, 0.000000000000000000 ) ) ;
#5832=CARTESIAN_POINT ( 'NONE',  ( -117.0000000000000000, -0.2735269159956698060, 3.990636919869545718 ) ) ;
#5850=DIRECTION ( 'NONE',  ( 0.000000000000000000, 0.5735764363510476027, -0.8191520442889906883 ) ) ;
#5859=EDGE_CURVE ( 'NONE', #9506, #3747, #7103, .T. ) ;
#5875=AXIS2_PLACEMENT_3D ( 'NONE', #5297, #8537, #4510 ) ;
#5900=CARTESIAN_POINT ( 'NONE',  ( -39.65557114539781480, 3.552635616211504477, -1.840410121656756326 ) ) ;
#5906=FACE_OUTER_BOUND ( 'NONE', #1640, .T. ) ;
#5910=CARTESIAN_POINT ( 'NONE',  ( -43.93820948810023452, 4.898587196589412829E-16, -4.000000000000000000 ) ) ;
#5928=DIRECTION ( 'NONE',  ( 1.000000000000000000, 0.000000000000000000, 0.000000000000000000 ) ) ;
#5929=ADVANCED_FACE ( 'NONE', ( #1732 ), #1680, .T. ) ;
#5948=CARTESIAN_POINT ( 'NONE',  ( -39.65624476065124782, -3.117691453623975484, -1.800000000000017586 ) ) ;
#5972=CARTESIAN_POINT ( 'NONE',  ( -8.000000000000000000, 0.000000000000000000, 0.000000000000000000 ) ) ;
#5980=EDGE_CURVE ( 'NONE', #6514, #7036, #722, .T. ) ;
#5983=DIRECTION ( 'NONE',  ( 0.000000000000000000, 0.000000000000000000, 1.000000000000000000 ) ) ;
#5990=ORIENTED_EDGE ( 'NONE', *, *, #10239, .F. ) ;
#5994=VERTEX_POINT ( 'NONE', #5910 ) ;
#6067=SPHERICAL_SURFACE ( 'NONE', #3654, 8.000000000000000000 ) ;
#6093=DIRECTION ( 'NONE',  ( -7.016001027857731783E-17, 0.8191520442889911324, -0.5735764363510471586 ) ) ;
#6107=VECTOR ( 'NONE', #3086, 1000.000000000000000 ) ;
#6115=AXIS2_PLACEMENT_3D ( 'NONE', #5825, #4974, #5769 ) ;
#6117=DIRECTION ( 'NONE',  ( 0.000000000000000000, 1.000000000000000000, 0.000000000000000000 ) ) ;
#6129=EDGE_LOOP ( 'NONE', ( #607, #1878, #4959, #597 ) ) ;
#6137=DIRECTION ( 'NONE',  ( -0.9805806756909200006, 0.1698415551216908848, -0.09805806756909091204 ) ) ;
#6195=EDGE_LOOP ( 'NONE', ( #5326, #7168, #9374, #4616, #784 ) ) ;
#6201=DIRECTION ( 'NONE',  ( 0.000000000000000000, 0.4226182617406934461, 0.9063077870366527122 ) ) ;
#6244=MECHANICAL_DESIGN_GEOMETRIC_PRESENTATION_REPRESENTATION('',(#1509),#1840);
#6291=DIRECTION ( 'NONE',  ( 0.1124875939035005490, -0.8966615917995903740, 0.4281874951574671795 ) ) ;
#6300=CARTESIAN_POINT ( 'NONE',  ( -38.96131932220313132, 0.2735269159956709717, 3.990636919869543942 ) ) ;
#6339=CARTESIAN_POINT ( 'NONE',  ( -1.071796769724492338, 0.000000000000000000, 0.000000000000000000 ) ) ;
#6345=LINE ( 'NONE', #3012, #10154 ) ;
#6397=DIRECTION ( 'NONE',  ( 0.000000000000000000, -0.9961946980917445460, -0.08715574274766943463 ) ) ;
#6418=DIRECTION ( 'NONE',  ( -6.485608039485835891E-17, -0.9063077870366466060, -0.4226182617407067132 ) ) ;
#6421=CIRCLE ( 'NONE', #506, 8.000000000000000000 ) ;
#6422=DIRECTION ( 'NONE',  ( 0.000000000000000000, -0.9961946980917445460, -0.08715574274766943463 ) ) ;
#6459=VECTOR ( 'NONE', #5244, 1000.000000000000000 ) ;
#6489=FACE_OUTER_BOUND ( 'NONE', #2168, .T. ) ;
#6491=ORIENTED_EDGE ( 'NONE', *, *, #4816, .F. ) ;
#6514=VERTEX_POINT ( 'NONE', #7605 ) ;
#6521=ADVANCED_FACE ( 'NONE', ( #3628 ), #8445, .F. ) ;
#6526=VECTOR ( 'NONE', #8232, 1000.000000000000000 ) ;
#6573=EDGE_CURVE ( 'NONE', #4377, #34, #2504, .T. ) ;
#6582=LINE ( 'NONE', #9065, #4364 ) ;
#6584=ORIENTED_EDGE ( 'NONE', *, *, #7644, .T. ) ;
#6629=EDGE_CURVE ( 'NONE', #9495, #8325, #2299, .T. ) ;
#6632=CARTESIAN_POINT ( 'NONE',  ( -38.96131932220313132, 3.319229491889295502, -2.232199717805805061 ) ) ;
#6673=CIRCLE ( 'NONE', #2101, 4.000000000000000000 ) ;
#6696=VERTEX_POINT ( 'NONE', #10255 ) ;
#6722=DIRECTION ( 'NONE',  ( -1.000000000000000000, -0.000000000000000000, -0.000000000000000000 ) ) ;
#6727=ORIENTED_EDGE ( 'NONE', *, *, #9489, .F. ) ;
#6738=DIRECTION ( 'NONE',  ( 0.000000000000000000, 0.000000000000000000, 1.000000000000000000 ) ) ;
#6739=ORIENTED_EDGE ( 'NONE', *, *, #9503, .T. ) ;
#6751=VECTOR ( 'NONE', #3241, 1000.000000000000000 ) ;
#6758=DIRECTION ( 'NONE',  ( 0.1124875939035005212, 0.8191520442889906883, 0.5624379695175003580 ) ) ;
#6763=LINE ( 'NONE', #6811, #1384 ) ;
#6777=ORIENTED_EDGE ( 'NONE', *, *, #6956, .F. ) ;
#6810=DIRECTION ( 'NONE',  ( 0.000000000000000000, 0.000000000000000000, 1.000000000000000000 ) ) ;
#6811=CARTESIAN_POINT ( 'NONE',  ( -39.00428932080996702, 3.065011249696406370, -1.804608920635871749 ) ) ;
#6812=ORIENTED_EDGE ( 'NONE', *, *, #2762, .F. ) ;
#6820=EDGE_CURVE ( 'NONE', #7406, #34, #4662, .T. ) ;
#6828=CARTESIAN_POINT ( 'NONE',  ( -117.0000000000000000, 0.000000000000000000, 0.000000000000000000 ) ) ;
#6839=CARTESIAN_POINT ( 'NONE',  ( -117.0000000000000000, 0.000000000000000000, 4.000000000000000000 ) ) ;
#6841=( BOUNDED_CURVE ( )  B_SPLINE_CURVE ( 3, ( #460, #310, #6868, #4383 ),
 .UNSPECIFIED., .F., .T. ) 
 B_SPLINE_CURVE_WITH_KNOTS ( ( 4, 4 ),
 ( 0.9691135948774319830, 1.037548729184187390 ),
 .UNSPECIFIED. ) 
 CURVE ( )  GEOMETRIC_REPRESENTATION_ITEM ( )  RATIONAL_B_SPLINE_CURVE ( ( 1.000000000000000000, 0.9996097574442918132, 0.9996097574442918132, 1.000000000000000000 ) ) 
 REPRESENTATION_ITEM ( '' )  );
#6844=ORIENTED_EDGE ( 'NONE', *, *, #3265, .F. ) ;
#6868=CARTESIAN_POINT ( 'NONE',  ( -39.65557114539780770, -3.370159726842522296, -2.156467633200152001 ) ) ;
#6874=AXIS2_PLACEMENT_3D ( 'NONE', #8455, #2729, #6810 ) ;
#6903=EDGE_LOOP ( 'NONE', ( #1450, #1180, #9624 ) ) ;
#6905=SHAPE_REPRESENTATION ( 'groove pin 01_iso_ISO 8739-M8x45-St', ( #4601 ), #1084 ) ;
#6907=DIRECTION ( 'NONE',  ( 1.000000000000000000, 0.000000000000000000, 0.000000000000000000 ) ) ;
#6916=AXIS2_PLACEMENT_3D ( 'NONE', #1616, #4843, #672 ) ;
#6923=FACE_OUTER_BOUND ( 'NONE', #10215, .T. ) ;
#6928=VERTEX_POINT ( 'NONE', #8949 ) ;
#6950=CARTESIAN_POINT ( 'NONE',  ( -8.000000000000000000, -1.691446717414637702, 1.184363742013801124 ) ) ;
#6956=EDGE_CURVE ( 'NONE', #3747, #1040, #2588, .T. ) ;
#6985=ORIENTED_EDGE ( 'NONE', *, *, #441, .T. ) ;
#7025=ORIENTED_EDGE ( 'NONE', *, *, #7734, .T. ) ;
#7028=CARTESIAN_POINT ( 'NONE',  ( -45.00000000000000000, 0.000000000000000000, 0.000000000000000000 ) ) ;
#7036=VERTEX_POINT ( 'NONE', #2001 ) ;
#7043=DIRECTION ( 'NONE',  ( -1.000000000000000000, -0.000000000000000000, -0.000000000000000000 ) ) ;
#7049=AXIS2_PLACEMENT_3D ( 'NONE', #7028, #9525, #10262 ) ;
#7065=ORIENTED_EDGE ( 'NONE', *, *, #9885, .T. ) ;
#7103=LINE ( 'NONE', #10336, #2336 ) ;
#7164=ADVANCED_FACE ( 'NONE', ( #22 ), #2454, .F. ) ;
#7168=ORIENTED_EDGE ( 'NONE', *, *, #5980, .T. ) ;
#7179=AXIS2_PLACEMENT_3D ( 'NONE', #6828, #6722, #4442 ) ;
#7182=PRODUCT_DEFINITION_FORMATION_WITH_SPECIFIED_SOURCE ( 'ANY', '', #5681, .NOT_KNOWN. ) ;
#7201=DIRECTION ( 'NONE',  ( 0.000000000000000000, 1.000000000000000000, 1.224646799147353207E-16 ) ) ;
#7202=ORIENTED_EDGE ( 'NONE', *, *, #155, .F. ) ;
#7218=CARTESIAN_POINT ( 'NONE',  ( -39.65624476065124782, -3.117691453623975484, -1.800000000000017586 ) ) ;
#7242=DIRECTION ( 'NONE',  ( 1.000000000000000000, 0.000000000000000000, 0.000000000000000000 ) ) ;
#7288=ORIENTED_EDGE ( 'NONE', *, *, #5859, .T. ) ;
#7330=( LENGTH_UNIT ( ) NAMED_UNIT ( * ) SI_UNIT ( .MILLI., .METRE. ) );
#7334=DIRECTION ( 'NONE',  ( 0.000000000000000000, 0.4226182617407067132, -0.9063077870366466060 ) ) ;
#7370=CARTESIAN_POINT ( 'NONE',  ( -39.00428932080996702, -3.065011249696382389, -1.804608920635915492 ) ) ;
#7374=DIRECTION ( 'NONE',  ( 1.000000000000000000, 0.000000000000000000, 0.000000000000000000 ) ) ;
#7406=VERTEX_POINT ( 'NONE', #3624 ) ;
#7407=AXIS2_PLACEMENT_3D ( 'NONE', #5203, #3727, #444 ) ;
#7481=CARTESIAN_POINT ( 'NONE',  ( -1.071796769724492338, 0.000000000000000000, 0.000000000000000000 ) ) ;
#7509=DIRECTION ( 'NONE',  ( -1.000000000000000000, -0.000000000000000000, -0.000000000000000000 ) ) ;
#7552=LINE ( 'NONE', #304, #10072 ) ;
#7589=ORIENTED_EDGE ( 'NONE', *, *, #2521, .F. ) ;
#7605=CARTESIAN_POINT ( 'NONE',  ( -43.93820948810023452, -4.000000000000000888, -4.898587196589413815E-16 ) ) ;
#7610=ORIENTED_EDGE ( 'NONE', *, *, #6573, .F. ) ;
#7644=EDGE_CURVE ( 'NONE', #3341, #3030, #5791, .T. ) ;
#7651=CIRCLE ( 'NONE', #6115, 4.000000000000000000 ) ;
#7662=DIRECTION ( 'NONE',  ( 0.000000000000000000, -0.9961946980917458783, 0.08715574274765483520 ) ) ;
#7666=VERTEX_POINT ( 'NONE', #7916 ) ;
#7667=( NAMED_UNIT ( * ) PLANE_ANGLE_UNIT ( ) SI_UNIT ( $, .RADIAN. ) );
#7670=ORIENTED_EDGE ( 'NONE', *, *, #4816, .T. ) ;
#7680=APPLICATION_CONTEXT ( 'automotive_design' ) ;
#7693=ORIENTED_EDGE ( 'NONE', *, *, #2905, .F. ) ;
#7700=CARTESIAN_POINT ( 'NONE',  ( -40.99999999999999289, -5.556536133988210224E-16, 4.000000000000005329 ) ) ;
#7703=AXIS2_PLACEMENT_3D ( 'NONE', #1383, #5103, #8339 ) ;
#7710=DIRECTION ( 'NONE',  ( 0.000000000000000000, 1.000000000000000000, 0.000000000000000000 ) ) ;
#7734=EDGE_CURVE ( 'NONE', #4613, #7406, #900, .T. ) ;
#7741=CARTESIAN_POINT ( 'NONE',  ( -39.00428932080996702, -3.095342794014893428, -1.752073144804227933 ) ) ;
#7810=VECTOR ( 'NONE', #9514, 1000.000000000000000 ) ;
#7811=CIRCLE ( 'NONE', #9859, 7.728925574020643730 ) ;
#7821=ORIENTED_EDGE ( 'NONE', *, *, #10425, .T. ) ;
#7867=VERTEX_POINT ( 'NONE', #2805 ) ;
#7868=CARTESIAN_POINT ( 'NONE',  ( -1.071796769724492338, -4.000000000000000000, -4.898587196589413815E-16 ) ) ;
#7870=CARTESIAN_POINT ( 'NONE',  ( -39.00436953563450970, -0.03089877619826558730, 3.555871974361681342 ) ) ;
#7916=CARTESIAN_POINT ( 'NONE',  ( -43.93820948810023452, 4.000000000000000888, 0.000000000000000000 ) ) ;
#7927=( BOUNDED_CURVE ( )  B_SPLINE_CURVE ( 3, ( #6632, #4299, #4247, #8629 ),
 .UNSPECIFIED., .F., .F. ) 
 B_SPLINE_CURVE_WITH_KNOTS ( ( 4, 4 ),
 ( 5.245636577995398397, 5.314071712302153472 ),
 .UNSPECIFIED. ) 
 CURVE ( )  GEOMETRIC_REPRESENTATION_ITEM ( )  RATIONAL_B_SPLINE_CURVE ( ( 1.000000000000000000, 0.9996097574442918132, 0.9996097574442918132, 1.000000000000000000 ) ) 
 REPRESENTATION_ITEM ( '' )  );
#7932=ORIENTED_EDGE ( 'NONE', *, *, #8199, .F. ) ;
#7984=CARTESIAN_POINT ( 'NONE',  ( -39.00428932080996702, 3.095342794014916965, -1.752073144804183080 ) ) ;
#7988=PLANE ( 'NONE',  #9079 ) ;
#8014=DIRECTION ( 'NONE',  ( -6.964995403156261684E-17, -0.08715574274766944851, 0.9961946980917446570 ) ) ;
#8017=DIRECTION ( 'NONE',  ( -1.000000000000000000, -0.000000000000000000, -0.000000000000000000 ) ) ;
#8041=ORIENTED_EDGE ( 'NONE', *, *, #2762, .T. ) ;
#8047=FACE_OUTER_BOUND ( 'NONE', #6903, .T. ) ;
#8056=CARTESIAN_POINT ( 'NONE',  ( -39.65557114539780770, -0.1824758893689537032, 3.996877754856925424 ) ) ;
#8063=EDGE_CURVE ( 'NONE', #2146, #4613, #9712, .T. ) ;
#8064=AXIS2_PLACEMENT_3D ( 'NONE', #8381, #8278, #6738 ) ;
#8131=CARTESIAN_POINT ( 'NONE',  ( -8.000000000000000000, 1.691446717414637479, 1.184363742013802900 ) ) ;
#8144=VERTEX_POINT ( 'NONE', #9865 ) ;
#8163=DIRECTION ( 'NONE',  ( 0.000000000000000000, 0.000000000000000000, 1.000000000000000000 ) ) ;
#8199=EDGE_CURVE ( 'NONE', #3747, #1722, #1047, .T. ) ;
#8232=DIRECTION ( 'NONE',  ( 0.08084652178105140863, 0.4212348471733803335, -0.9033410449230815376 ) ) ;
#8278=DIRECTION ( 'NONE',  ( -1.000000000000000000, -0.000000000000000000, -0.000000000000000000 ) ) ;
#8290=ADVANCED_FACE ( 'NONE', ( #370 ), #5337, .T. ) ;
#8325=VERTEX_POINT ( 'NONE', #9158 ) ;
#8339=DIRECTION ( 'NONE',  ( 0.000000000000000000, 0.000000000000000000, 1.000000000000000000 ) ) ;
#8373=CARTESIAN_POINT ( 'NONE',  ( -117.0000000000000000, 4.898587196589412829E-16, -4.000000000000000000 ) ) ;
#8381=CARTESIAN_POINT ( 'NONE',  ( -1.071796769724492338, 0.000000000000000000, 0.000000000000000000 ) ) ;
#8420=CARTESIAN_POINT ( 'NONE',  ( -38.96131932220313132, -0.2735269159956721374, 3.990636919869543942 ) ) ;
#8445=PLANE ( 'NONE',  #2229 ) ;
#8455=CARTESIAN_POINT ( 'NONE',  ( -45.00000000000000000, 0.000000000000000000, 0.000000000000000000 ) ) ;
#8475=ORIENTED_EDGE ( 'NONE', *, *, #772, .F. ) ;
#8510=ORIENTED_EDGE ( 'NONE', *, *, #2684, .F. ) ;
#8514=SHAPE_REPRESENTATION_RELATIONSHIP ( 'NONE' , 'NONE' ,  #6905, #3680 ) ;
#8524=PRODUCT_DEFINITION ( 'UNKNOWN', '', #7182, #5044 ) ;
#8528=CARTESIAN_POINT ( 'NONE',  ( -39.00000000000000000, 3.117691453623999909, -1.799999999999972733 ) ) ;
#8532=DIRECTION ( 'NONE',  ( -7.493424318096922963E-17, 0.9063077870366528233, -0.4226182617406935016 ) ) ;
#8537=DIRECTION ( 'NONE',  ( -7.016001027857731783E-17, 0.8191520442889911324, -0.5735764363510471586 ) ) ;
#8551=DIRECTION ( 'NONE',  ( 1.000000000000000000, 0.000000000000000000, 0.000000000000000000 ) ) ;
#8557=LINE ( 'NONE', #4636, #10110 ) ;
#8586=CARTESIAN_POINT ( 'NONE',  ( 0.000000000000000000, 0.000000000000000000, 0.000000000000000000 ) ) ;
#8589=DIRECTION ( 'NONE',  ( -7.493424318096921731E-17, 0.9063077870366529343, -0.4226182617406935016 ) ) ;
#8610=CARTESIAN_POINT ( 'NONE',  ( -38.99999999999999289, -5.592496027482437178E-16, 3.600000000000004530 ) ) ;
#8629=CARTESIAN_POINT ( 'NONE',  ( -40.99999999999999289, 3.464101615137777923, -1.999999999999970468 ) ) ;
#8638=FACE_OUTER_BOUND ( 'NONE', #2976, .T. ) ;
#8682=DIRECTION ( 'NONE',  ( -6.964995403156261684E-17, -0.08715574274766943463, 0.9961946980917445460 ) ) ;
#8686=ORIENTED_EDGE ( 'NONE', *, *, #4012, .T. ) ;
#8735=CARTESIAN_POINT ( 'NONE',  ( -37.01000625782472753, 0.000000000000000000, 0.000000000000000000 ) ) ;
#8777=ADVANCED_FACE ( 'NONE', ( #5906 ), #308, .T. ) ;
#8781=DIRECTION ( 'NONE',  ( -0.000000000000000000, 0.000000000000000000, 1.000000000000000000 ) ) ;
#8824=ORIENTED_EDGE ( 'NONE', *, *, #8063, .F. ) ;
#8832=DIRECTION ( 'NONE',  ( 0.000000000000000000, -0.4309225046084370070, -0.9023889377768278264 ) ) ;
#8929=EDGE_LOOP ( 'NONE', ( #1880, #315, #10243, #9558 ) ) ;
#8949=CARTESIAN_POINT ( 'NONE',  ( 0.000000000000000000, 4.898587196589412829E-16, 0.000000000000000000 ) ) ;
#8957=EDGE_LOOP ( 'NONE', ( #9421, #7821, #2329, #2909, #3618, #8475, #5274, #962, #7025, #9328, #7610, #5325, #4370 ) ) ;
#8961=PLANE ( 'NONE',  #4865 ) ;
#9016=LINE ( 'NONE', #2602, #5207 ) ;
#9065=CARTESIAN_POINT ( 'NONE',  ( -39.00428932080996702, -3.065011249696382389, -1.804608920635915492 ) ) ;
#9076=AXIS2_PLACEMENT_3D ( 'NONE', #2059, #8532, #1270 ) ;
#9079=AXIS2_PLACEMENT_3D ( 'NONE', #10434, #8682, #6397 ) ;
#9097=EDGE_CURVE ( 'NONE', #7666, #5994, #6673, .T. ) ;
#9138=CARTESIAN_POINT ( 'NONE',  ( -38.96131932220313132, 3.592756407884963199, -1.758437202063674487 ) ) ;
#9158=CARTESIAN_POINT ( 'NONE',  ( -1.071796769724492338, -3.592756407884937442, -1.758437202063728222 ) ) ;
#9162=VERTEX_POINT ( 'NONE', #4511 ) ;
#9180=VERTEX_POINT ( 'NONE', #10185 ) ;
#9189=DIRECTION ( 'NONE',  ( 0.000000000000000000, 0.000000000000000000, 1.000000000000000000 ) ) ;
#9192=ORIENTED_EDGE ( 'NONE', *, *, #5596, .F. ) ;
#9199=CARTESIAN_POINT ( 'NONE',  ( -39.00436953563450970, 0.03089877619826473382, 3.555871974361681342 ) ) ;
#9200=ADVANCED_FACE ( 'NONE', ( #8638 ), #4612, .T. ) ;
#9201=CARTESIAN_POINT ( 'NONE',  ( -8.000000000000000000, -0.1799657291978226659, -2.057017697435776338 ) ) ;
#9219=ADVANCED_FACE ( 'NONE', ( #8047 ), #3885, .T. ) ;
#9253=DIRECTION ( 'NONE',  ( -0.000000000000000000, 0.000000000000000000, -1.000000000000000000 ) ) ;
#9266=ORIENTED_EDGE ( 'NONE', *, *, #3390, .T. ) ;
#9267=DIRECTION ( 'NONE',  ( 0.000000000000000000, 0.000000000000000000, 1.000000000000000000 ) ) ;
#9268=AXIS2_PLACEMENT_3D ( 'NONE', #4559, #8589, #6201 ) ;
#9309=DIRECTION ( 'NONE',  ( 0.000000000000000000, -0.5660304919045656691, 0.8243843049417398650 ) ) ;
#9310=CARTESIAN_POINT ( 'NONE',  ( -8.000000000000000000, 0.000000000000000000, 0.000000000000000000 ) ) ;
#9328=ORIENTED_EDGE ( 'NONE', *, *, #6820, .T. ) ;
#9329=FACE_OUTER_BOUND ( 'NONE', #6129, .T. ) ;
#9349=VERTEX_POINT ( 'NONE', #2595 ) ;
#9374=ORIENTED_EDGE ( 'NONE', *, *, #10315, .T. ) ;
#9421=ORIENTED_EDGE ( 'NONE', *, *, #2583, .T. ) ;
#9449=CIRCLE ( 'NONE', #4697, 7.728925574020643730 ) ;
#9465=AXIS2_PLACEMENT_3D ( 'NONE', #8131, #980, #5850 ) ;
#9489=EDGE_CURVE ( 'NONE', #8144, #4377, #423, .T. ) ;
#9495=VERTEX_POINT ( 'NONE', #326 ) ;
#9503=EDGE_CURVE ( 'NONE', #9495, #7867, #2843, .T. ) ;
#9506=VERTEX_POINT ( 'NONE', #8420 ) ;
#9508=CARTESIAN_POINT ( 'NONE',  ( -38.96131932220313132, -0.2735269159956721374, 3.990636919869543942 ) ) ;
#9512=DIRECTION ( 'NONE',  ( 0.000000000000000000, 0.000000000000000000, -1.000000000000000000 ) ) ;
#9514=DIRECTION ( 'NONE',  ( 1.000000000000000000, 0.000000000000000000, 0.000000000000000000 ) ) ;
#9525=DIRECTION ( 'NONE',  ( -1.000000000000000000, -0.000000000000000000, -0.000000000000000000 ) ) ;
#9545=ORIENTED_EDGE ( 'NONE', *, *, #5859, .F. ) ;
#9548=ORIENTED_EDGE ( 'NONE', *, *, #5629, .F. ) ;
#9558=ORIENTED_EDGE ( 'NONE', *, *, #9885, .F. ) ;
#9563=CARTESIAN_POINT ( 'NONE',  ( -1.071796769724492338, -0.2735269159956698060, 3.990636919869545718 ) ) ;
#9589=ORIENTED_EDGE ( 'NONE', *, *, #5041, .T. ) ;
#9624=ORIENTED_EDGE ( 'NONE', *, *, #9489, .T. ) ;
#9648=CARTESIAN_POINT ( 'NONE',  ( -1.071796769724492338, 4.000000000000000000, 0.000000000000000000 ) ) ;
#9665=ORIENTED_EDGE ( 'NONE', *, *, #6629, .T. ) ;
#9675=EDGE_LOOP ( 'NONE', ( #501, #6985, #8824, #2195, #5093, #6844 ) ) ;
#9684=DIRECTION ( 'NONE',  ( 0.000000000000000000, 0.000000000000000000, 1.000000000000000000 ) ) ;
#9712=CIRCLE ( 'NONE', #5128, 3.999999999999999112 ) ;
#9802=DIRECTION ( 'NONE',  ( -0.000000000000000000, 0.000000000000000000, -1.000000000000000000 ) ) ;
#9825=DIRECTION ( 'NONE',  ( 0.08084652178105142251, -0.9929337167712581902, 0.08687044385014237868 ) ) ;
#9859=AXIS2_PLACEMENT_3D ( 'NONE', #9201, #5167, #7662 ) ;
#9865=CARTESIAN_POINT ( 'NONE',  ( -39.00000000000000000, 3.117691453623999909, -1.799999999999972733 ) ) ;
#9874=EDGE_CURVE ( 'NONE', #34, #8144, #6763, .T. ) ;
#9875=DIRECTION ( 'NONE',  ( 0.1124875939035004796, -0.07750954751059241365, -0.9906254646749721449 ) ) ;
#9877=DIRECTION ( 'NONE',  ( -1.000000000000000000, -0.000000000000000000, -0.000000000000000000 ) ) ;
#9885=EDGE_CURVE ( 'NONE', #8325, #723, #7811, .T. ) ;
#9893=EDGE_CURVE ( 'NONE', #7867, #6696, #6841, .T. ) ;
#9956=CIRCLE ( 'NONE', #3342, 4.000000000000000000 ) ;
#9982=CIRCLE ( 'NONE', #9465, 7.728925574020641953 ) ;
#10020=CARTESIAN_POINT ( 'NONE',  ( -38.96131932220313132, -3.592756407884938330, -1.758437202063725779 ) ) ;
#10026=VECTOR ( 'NONE', #3664, 1000.000000000000000 ) ;
#10050=DIRECTION ( 'NONE',  ( 0.000000000000000000, 1.000000000000000000, 0.000000000000000000 ) ) ;
#10072=VECTOR ( 'NONE', #3526, 1000.000000000000000 ) ;
#10096=DIRECTION ( 'NONE',  ( -7.061912783291096091E-17, 0.08715574274765486296, 0.9961946980917458783 ) ) ;
#10110=VECTOR ( 'NONE', #1461, 1000.000000000000114 ) ;
#10154=VECTOR ( 'NONE', #7043, 1000.000000000000000 ) ;
#10166=VERTEX_POINT ( 'NONE', #9563 ) ;
#10176=EDGE_CURVE ( 'NONE', #289, #723, #3940, .T. ) ;
#10185=CARTESIAN_POINT ( 'NONE',  ( -1.071796769724492338, 4.898587196589411843E-16, -3.999999999999999112 ) ) ;
#10215=EDGE_LOOP ( 'NONE', ( #2040, #3799, #9192, #7065, #8686, #9548, #10328, #6584, #1054, #4867 ) ) ;
#10225=VECTOR ( 'NONE', #268, 1000.000000000000114 ) ;
#10239=EDGE_CURVE ( 'NONE', #1722, #9506, #2908, .T. ) ;
#10243=ORIENTED_EDGE ( 'NONE', *, *, #10176, .T. ) ;
#10255=CARTESIAN_POINT ( 'NONE',  ( -38.96131932220313132, -3.319229491889264416, -2.232199717805851691 ) ) ;
#10262=DIRECTION ( 'NONE',  ( 0.000000000000000000, 0.000000000000000000, 1.000000000000000000 ) ) ;
#10275=DIRECTION ( 'NONE',  ( -6.485608039485835891E-17, -0.9063077870366466060, -0.4226182617407067132 ) ) ;
#10288=PLANE ( 'NONE',  #9076 ) ;
#10310=CARTESIAN_POINT ( 'NONE',  ( -8.000000000000000000, 1.871412446612461755, 0.8726539554219916450 ) ) ;
#10315=EDGE_CURVE ( 'NONE', #7036, #7666, #7651, .T. ) ;
#10328=ORIENTED_EDGE ( 'NONE', *, *, #2583, .F. ) ;
#10334=FACE_OUTER_BOUND ( 'NONE', #2867, .T. ) ;
#10336=CARTESIAN_POINT ( 'NONE',  ( -39.00436953563450970, 0.03089877619826473382, 3.555871974361681342 ) ) ;
#10355=CARTESIAN_POINT ( 'NONE',  ( -1.071796769724492338, -3.319229491889267081, -2.232199717805850803 ) ) ;
#10356=DIRECTION ( 'NONE',  ( 0.000000000000000000, 0.4226182617407066577, -0.9063077870366466060 ) ) ;
#10357=FACE_OUTER_BOUND ( 'NONE', #1373, .T. ) ;
#10364=PLANE ( 'NONE',  #5533 ) ;
#10375=AXIS2_PLACEMENT_3D ( 'NONE', #5064, #7509, #5751 ) ;
#10376=ORIENTED_EDGE ( 'NONE', *, *, #772, .T. ) ;
#10425=EDGE_CURVE ( 'NONE', #9180, #5994, #481, .T. ) ;
#10432=AXIS2_PLACEMENT_3D ( 'NONE', #7984, #2267, #3962 ) ;
#10434=CARTESIAN_POINT ( 'NONE',  ( -39.65624476065125492, 3.117691453623999909, -1.799999999999972955 ) ) ;
#10444=DIRECTION ( 'NONE',  ( 0.000000000000000000, 0.000000000000000000, 1.000000000000000000 ) ) ;
#10462=VECTOR ( 'NONE', #6907, 1000.000000000000000 ) ;
#10477=EDGE_CURVE ( 'NONE', #1722, #7036, #3502, .T. ) ;
#10512=COLOUR_RGB('Grey',0.48,0.52,0.57);
#10513=FILL_AREA_STYLE_COLOUR('',#10512);
#10514=FILL_AREA_STYLE('',(#10513));
#10515=SURFACE_STYLE_FILL_AREA(#10514);
#10516=SURFACE_SIDE_STYLE('',(#10515));
#10517=SURFACE_STYLE_USAGE(.BOTH.,#10516);
#10518=PRESENTATION_STYLE_ASSIGNMENT((#10517));
ENDSEC;
END-ISO-10303-21;
